ISO-10303-21;
HEADER;
/* Generated by software containing ST-Developer
 * from STEP Tools, Inc. (www.steptools.com) 
 */

FILE_DESCRIPTION(
/* description */ (''),
/* implementation_level */ '2;1');

FILE_NAME(
/* name */ 'Flat Washer - M6.step',
/* time_stamp */ '2026-10-29T16:43:51-07:00',
/* author */ (''),
/* organization */ (''),
/* preprocessor_version */ 'ST-DEVELOPER v20.2',
/* originating_system */ 'Autodesk Translation Framework v15.17.0.0',
/* authorisation */ '');

FILE_SCHEMA (('AUTOMOTIVE_DESIGN { 1 0 10303 214 3 1 1 }'));
ENDSEC;

DATA;
#10=MECHANICAL_DESIGN_GEOMETRIC_PRESENTATION_REPRESENTATION('',(#386),#10292);
#340=SHAPE_REPRESENTATION_RELATIONSHIP('SRR','None',#10438,#363);
#363=ADVANCED_BREP_SHAPE_REPRESENTATION('',(#405),#10290);
#386=STYLED_ITEM('',(#10635),#405);
#405=MANIFOLD_SOLID_BREP('Body1',#5032);
#528=FACE_BOUND('',#1390,.T.);
#529=FACE_BOUND('',#1392,.T.);
#697=PLANE('',#5813);
#698=PLANE('',#5814);
#977=FACE_OUTER_BOUND('',#1387,.T.);
#978=FACE_OUTER_BOUND('',#1388,.T.);
#979=FACE_OUTER_BOUND('',#1389,.T.);
#980=FACE_OUTER_BOUND('',#1391,.T.);
#1387=EDGE_LOOP('',(#4561,#4562,#4563,#4564));
#1388=EDGE_LOOP('',(#4565,#4566,#4567,#4568));
#1389=EDGE_LOOP('',(#4569));
#1390=EDGE_LOOP('',(#4570));
#1391=EDGE_LOOP('',(#4571));
#1392=EDGE_LOOP('',(#4572));
#1777=LINE('',#10134,#2169);
#1778=LINE('',#10140,#2170);
#2169=VECTOR('',#7270,0.32);
#2170=VECTOR('',#7277,0.6);
#2382=CIRCLE('',#5808,0.32);
#2383=CIRCLE('',#5809,0.32);
#2384=CIRCLE('',#5811,0.6);
#2385=CIRCLE('',#5812,0.6);
#2771=VERTEX_POINT('',#10131);
#2772=VERTEX_POINT('',#10133);
#2773=VERTEX_POINT('',#10137);
#2774=VERTEX_POINT('',#10139);
#3371=EDGE_CURVE('',#2771,#2771,#2382,.T.);
#3372=EDGE_CURVE('',#2771,#2772,#1777,.T.);
#3373=EDGE_CURVE('',#2772,#2772,#2383,.T.);
#3374=EDGE_CURVE('',#2773,#2773,#2384,.T.);
#3375=EDGE_CURVE('',#2773,#2774,#1778,.T.);
#3376=EDGE_CURVE('',#2774,#2774,#2385,.T.);
#4561=ORIENTED_EDGE('',*,*,#3371,.F.);
#4562=ORIENTED_EDGE('',*,*,#3372,.T.);
#4563=ORIENTED_EDGE('',*,*,#3373,.T.);
#4564=ORIENTED_EDGE('',*,*,#3372,.F.);
#4565=ORIENTED_EDGE('',*,*,#3374,.F.);
#4566=ORIENTED_EDGE('',*,*,#3375,.T.);
#4567=ORIENTED_EDGE('',*,*,#3376,.T.);
#4568=ORIENTED_EDGE('',*,*,#3375,.F.);
#4569=ORIENTED_EDGE('',*,*,#3374,.T.);
#4570=ORIENTED_EDGE('',*,*,#3371,.T.);
#4571=ORIENTED_EDGE('',*,*,#3376,.F.);
#4572=ORIENTED_EDGE('',*,*,#3373,.F.);
#4715=CYLINDRICAL_SURFACE('',#5807,0.32);
#4716=CYLINDRICAL_SURFACE('',#5810,0.6);
#4986=ADVANCED_FACE('',(#977),#4715,.F.);
#4987=ADVANCED_FACE('',(#978),#4716,.T.);
#4988=ADVANCED_FACE('',(#979,#528),#697,.T.);
#4989=ADVANCED_FACE('',(#980,#529),#698,.F.);
#5032=CLOSED_SHELL('',(#4986,#4987,#4988,#4989));
#5806=AXIS2_PLACEMENT_3D('',#10129,#7264,#7265);
#5807=AXIS2_PLACEMENT_3D('',#10130,#7266,#7267);
#5808=AXIS2_PLACEMENT_3D('',#10132,#7268,#7269);
#5809=AXIS2_PLACEMENT_3D('',#10135,#7271,#7272);
#5810=AXIS2_PLACEMENT_3D('',#10136,#7273,#7274);
#5811=AXIS2_PLACEMENT_3D('',#10138,#7275,#7276);
#5812=AXIS2_PLACEMENT_3D('',#10141,#7278,#7279);
#5813=AXIS2_PLACEMENT_3D('',#10142,#7280,#7281);
#5814=AXIS2_PLACEMENT_3D('',#10143,#7282,#7283);
#7264=DIRECTION('axis',(0.,0.,1.));
#7265=DIRECTION('refdir',(1.,0.,0.));
#7266=DIRECTION('center_axis',(0.,1.,0.));
#7267=DIRECTION('ref_axis',(1.,0.,0.));
#7268=DIRECTION('center_axis',(0.,-1.,0.));
#7269=DIRECTION('ref_axis',(1.,0.,0.));
#7270=DIRECTION('',(0.,-1.,0.));
#7271=DIRECTION('center_axis',(0.,-1.,0.));
#7272=DIRECTION('ref_axis',(1.,0.,0.));
#7273=DIRECTION('center_axis',(0.,1.,0.));
#7274=DIRECTION('ref_axis',(1.,0.,0.));
#7275=DIRECTION('center_axis',(0.,1.,0.));
#7276=DIRECTION('ref_axis',(1.,0.,0.));
#7277=DIRECTION('',(0.,-1.,0.));
#7278=DIRECTION('center_axis',(0.,1.,0.));
#7279=DIRECTION('ref_axis',(1.,0.,0.));
#7280=DIRECTION('center_axis',(0.,1.,0.));
#7281=DIRECTION('ref_axis',(1.,0.,0.));
#7282=DIRECTION('center_axis',(0.,1.,0.));
#7283=DIRECTION('ref_axis',(1.,0.,0.));
#10129=CARTESIAN_POINT('',(0.,0.,0.));
#10130=CARTESIAN_POINT('Origin',(0.,0.,0.));
#10131=CARTESIAN_POINT('',(-0.32,0.16,3.91886975727153E-17));
#10132=CARTESIAN_POINT('Origin',(0.,0.16,0.));
#10133=CARTESIAN_POINT('',(-0.32,0.,3.91886975727153E-17));
#10134=CARTESIAN_POINT('',(-0.32,0.,3.91886975727153E-17));
#10135=CARTESIAN_POINT('Origin',(0.,0.,0.));
#10136=CARTESIAN_POINT('Origin',(0.,0.,0.));
#10137=CARTESIAN_POINT('',(-0.6,0.16,7.34788079488412E-17));
#10138=CARTESIAN_POINT('Origin',(0.,0.16,0.));
#10139=CARTESIAN_POINT('',(-0.6,0.,7.34788079488412E-17));
#10140=CARTESIAN_POINT('',(-0.6,0.,7.34788079488412E-17));
#10141=CARTESIAN_POINT('Origin',(0.,0.,0.));
#10142=CARTESIAN_POINT('Origin',(0.,0.16,0.));
#10143=CARTESIAN_POINT('Origin',(0.,0.,0.));
#10262=UNCERTAINTY_MEASURE_WITH_UNIT(LENGTH_MEASURE(0.001),#10293,
'DISTANCE_ACCURACY_VALUE',
'Maximum model space distance between geometric entities at asserted c
onnectivities');
#10264=UNCERTAINTY_MEASURE_WITH_UNIT(LENGTH_MEASURE(0.001),#10293,
'DISTANCE_ACCURACY_VALUE',
'Maximum model space distance between geometric entities at asserted c
onnectivities');
#10290=(
GEOMETRIC_REPRESENTATION_CONTEXT(3)
GLOBAL_UNCERTAINTY_ASSIGNED_CONTEXT((#10262))
GLOBAL_UNIT_ASSIGNED_CONTEXT((#10293,#10295,#10296))
REPRESENTATION_CONTEXT('','3D')
);
#10292=(
GEOMETRIC_REPRESENTATION_CONTEXT(3)
GLOBAL_UNCERTAINTY_ASSIGNED_CONTEXT((#10264))
GLOBAL_UNIT_ASSIGNED_CONTEXT((#10293,#10295,#10296))
REPRESENTATION_CONTEXT('','3D')
);
#10293=(
LENGTH_UNIT()
NAMED_UNIT(*)
SI_UNIT(.CENTI.,.METRE.)
);
#10295=(
NAMED_UNIT(*)
PLANE_ANGLE_UNIT()
SI_UNIT($,.RADIAN.)
);
#10296=(
NAMED_UNIT(*)
SI_UNIT($,.STERADIAN.)
SOLID_ANGLE_UNIT()
);
#10322=SHAPE_DEFINITION_REPRESENTATION(#10388,#10438);
#10388=PRODUCT_DEFINITION_SHAPE('',$,#10466);
#10438=SHAPE_REPRESENTATION('',(#5806),#10290);
#10440=PRODUCT_DEFINITION_CONTEXT('part definition',#10523,'design');
#10466=PRODUCT_DEFINITION('Flat Washer - M6','Flat Washer - M6',
#10493,#10440);
#10493=PRODUCT_DEFINITION_FORMATION('',$,#10550);
#10523=APPLICATION_CONTEXT(
'Core Data for Automotive Mechanical Design Process');
#10524=PRODUCT_CONTEXT('part definition',#10523,'mechanical');
#10550=PRODUCT('Flat Washer - M6','Flat Washer - M6',
'Flat Washer - M6',(#10524));
#10629=COLOUR_RGB('Black',0.12,0.14,0.17);
#10630=FILL_AREA_STYLE_COLOUR('',#10629);
#10631=FILL_AREA_STYLE('',(#10630));
#10632=SURFACE_STYLE_FILL_AREA(#10631);
#10633=SURFACE_SIDE_STYLE('',(#10632));
#10634=SURFACE_STYLE_USAGE(.BOTH.,#10633);
#10635=PRESENTATION_STYLE_ASSIGNMENT((#10634));
ENDSEC;
END-ISO-10303-21;
